ISO-10303-21;
HEADER;
/* Generated by software containing ST-Developer
 * from STEP Tools, Inc. (www.steptools.com) 
 */

FILE_DESCRIPTION(
/* description */ ('Worm-less right-angle friction wheel drive'),
/* implementation_level */ '2;1');

FILE_NAME(
/* name */ 'Bearing cap (5).step',
/* time_stamp */ '2026-10-28T03:22:36-07:00',
/* author */ (''),
/* organization */ (''),
/* preprocessor_version */ 'ST-DEVELOPER v20.2',
/* originating_system */ 'Autodesk Translation Framework v15.17.0.0',
/* authorisation */ '');

FILE_SCHEMA (('AUTOMOTIVE_DESIGN { 1 0 10303 214 3 1 1 }'));
ENDSEC;

DATA;
#10=MECHANICAL_DESIGN_GEOMETRIC_PRESENTATION_REPRESENTATION('',(#623),#17046);
#529=SHAPE_REPRESENTATION_RELATIONSHIP('SRR','None',#17272,#576);
#576=ADVANCED_BREP_SHAPE_REPRESENTATION('',(#677),#17008);
#623=STYLED_ITEM('',(#17591),#677);
#677=MANIFOLD_SOLID_BREP('Body1',#8178);
#848=FACE_BOUND('',#1968,.T.);
#849=FACE_BOUND('',#1972,.T.);
#850=FACE_BOUND('',#1973,.T.);
#851=FACE_BOUND('',#1974,.T.);
#852=FACE_BOUND('',#1975,.T.);
#853=FACE_BOUND('',#1976,.T.);
#854=FACE_BOUND('',#1978,.T.);
#855=FACE_BOUND('',#1979,.T.);
#856=FACE_BOUND('',#1980,.T.);
#857=FACE_BOUND('',#1981,.T.);
#858=FACE_BOUND('',#1982,.T.);
#1029=PLANE('',#9083);
#1030=PLANE('',#9090);
#1031=PLANE('',#9091);
#1363=FACE_OUTER_BOUND('',#1962,.T.);
#1364=FACE_OUTER_BOUND('',#1963,.T.);
#1365=FACE_OUTER_BOUND('',#1964,.T.);
#1366=FACE_OUTER_BOUND('',#1965,.T.);
#1367=FACE_OUTER_BOUND('',#1966,.T.);
#1368=FACE_OUTER_BOUND('',#1967,.T.);
#1369=FACE_OUTER_BOUND('',#1969,.T.);
#1370=FACE_OUTER_BOUND('',#1970,.T.);
#1371=FACE_OUTER_BOUND('',#1971,.T.);
#1372=FACE_OUTER_BOUND('',#1977,.T.);
#1962=EDGE_LOOP('',(#6290,#6291,#6292,#6293));
#1963=EDGE_LOOP('',(#6294,#6295,#6296,#6297));
#1964=EDGE_LOOP('',(#6298,#6299,#6300,#6301));
#1965=EDGE_LOOP('',(#6302,#6303,#6304,#6305));
#1966=EDGE_LOOP('',(#6306,#6307,#6308,#6309));
#1967=EDGE_LOOP('',(#6310));
#1968=EDGE_LOOP('',(#6311));
#1969=EDGE_LOOP('',(#6312,#6313,#6314,#6315));
#1970=EDGE_LOOP('',(#6316,#6317,#6318,#6319));
#1971=EDGE_LOOP('',(#6320));
#1972=EDGE_LOOP('',(#6321));
#1973=EDGE_LOOP('',(#6322));
#1974=EDGE_LOOP('',(#6323));
#1975=EDGE_LOOP('',(#6324));
#1976=EDGE_LOOP('',(#6325));
#1977=EDGE_LOOP('',(#6326));
#1978=EDGE_LOOP('',(#6327));
#1979=EDGE_LOOP('',(#6328));
#1980=EDGE_LOOP('',(#6329));
#1981=EDGE_LOOP('',(#6330));
#1982=EDGE_LOOP('',(#6331));
#2599=LINE('',#13179,#3139);
#2600=LINE('',#13185,#3140);
#2601=LINE('',#13191,#3141);
#2602=LINE('',#13197,#3142);
#2603=LINE('',#13203,#3143);
#2604=LINE('',#13211,#3144);
#2605=LINE('',#13216,#3145);
#3139=VECTOR('',#10651,0.225);
#3140=VECTOR('',#10658,0.225);
#3141=VECTOR('',#10665,0.225);
#3142=VECTOR('',#10672,0.225);
#3143=VECTOR('',#10679,1.59);
#3144=VECTOR('',#10690,1.2);
#3145=VECTOR('',#10695,2.4);
#3613=CIRCLE('',#9069,0.225);
#3614=CIRCLE('',#9070,0.225);
#3615=CIRCLE('',#9072,0.225);
#3616=CIRCLE('',#9073,0.225);
#3617=CIRCLE('',#9075,0.225);
#3618=CIRCLE('',#9076,0.225);
#3619=CIRCLE('',#9078,0.225);
#3620=CIRCLE('',#9079,0.225);
#3621=CIRCLE('',#9081,1.59);
#3622=CIRCLE('',#9082,1.59);
#3623=CIRCLE('',#9084,1.2);
#3624=CIRCLE('',#9086,1.2);
#3625=CIRCLE('',#9088,2.4);
#3626=CIRCLE('',#9089,2.4);
#4121=VERTEX_POINT('',#13176);
#4122=VERTEX_POINT('',#13178);
#4123=VERTEX_POINT('',#13182);
#4124=VERTEX_POINT('',#13184);
#4125=VERTEX_POINT('',#13188);
#4126=VERTEX_POINT('',#13190);
#4127=VERTEX_POINT('',#13194);
#4128=VERTEX_POINT('',#13196);
#4129=VERTEX_POINT('',#13200);
#4130=VERTEX_POINT('',#13202);
#4131=VERTEX_POINT('',#13206);
#4132=VERTEX_POINT('',#13209);
#4133=VERTEX_POINT('',#13213);
#4134=VERTEX_POINT('',#13215);
#4914=EDGE_CURVE('',#4121,#4121,#3613,.T.);
#4915=EDGE_CURVE('',#4121,#4122,#2599,.T.);
#4916=EDGE_CURVE('',#4122,#4122,#3614,.T.);
#4917=EDGE_CURVE('',#4123,#4123,#3615,.T.);
#4918=EDGE_CURVE('',#4123,#4124,#2600,.T.);
#4919=EDGE_CURVE('',#4124,#4124,#3616,.T.);
#4920=EDGE_CURVE('',#4125,#4125,#3617,.T.);
#4921=EDGE_CURVE('',#4125,#4126,#2601,.T.);
#4922=EDGE_CURVE('',#4126,#4126,#3618,.T.);
#4923=EDGE_CURVE('',#4127,#4127,#3619,.T.);
#4924=EDGE_CURVE('',#4127,#4128,#2602,.T.);
#4925=EDGE_CURVE('',#4128,#4128,#3620,.T.);
#4926=EDGE_CURVE('',#4129,#4129,#3621,.T.);
#4927=EDGE_CURVE('',#4129,#4130,#2603,.T.);
#4928=EDGE_CURVE('',#4130,#4130,#3622,.T.);
#4929=EDGE_CURVE('',#4131,#4131,#3623,.T.);
#4930=EDGE_CURVE('',#4132,#4132,#3624,.T.);
#4931=EDGE_CURVE('',#4132,#4131,#2604,.T.);
#4932=EDGE_CURVE('',#4133,#4133,#3625,.T.);
#4933=EDGE_CURVE('',#4133,#4134,#2605,.T.);
#4934=EDGE_CURVE('',#4134,#4134,#3626,.T.);
#6290=ORIENTED_EDGE('',*,*,#4914,.F.);
#6291=ORIENTED_EDGE('',*,*,#4915,.T.);
#6292=ORIENTED_EDGE('',*,*,#4916,.F.);
#6293=ORIENTED_EDGE('',*,*,#4915,.F.);
#6294=ORIENTED_EDGE('',*,*,#4917,.F.);
#6295=ORIENTED_EDGE('',*,*,#4918,.T.);
#6296=ORIENTED_EDGE('',*,*,#4919,.F.);
#6297=ORIENTED_EDGE('',*,*,#4918,.F.);
#6298=ORIENTED_EDGE('',*,*,#4920,.F.);
#6299=ORIENTED_EDGE('',*,*,#4921,.T.);
#6300=ORIENTED_EDGE('',*,*,#4922,.F.);
#6301=ORIENTED_EDGE('',*,*,#4921,.F.);
#6302=ORIENTED_EDGE('',*,*,#4923,.F.);
#6303=ORIENTED_EDGE('',*,*,#4924,.T.);
#6304=ORIENTED_EDGE('',*,*,#4925,.F.);
#6305=ORIENTED_EDGE('',*,*,#4924,.F.);
#6306=ORIENTED_EDGE('',*,*,#4926,.F.);
#6307=ORIENTED_EDGE('',*,*,#4927,.T.);
#6308=ORIENTED_EDGE('',*,*,#4928,.T.);
#6309=ORIENTED_EDGE('',*,*,#4927,.F.);
#6310=ORIENTED_EDGE('',*,*,#4928,.F.);
#6311=ORIENTED_EDGE('',*,*,#4929,.F.);
#6312=ORIENTED_EDGE('',*,*,#4930,.F.);
#6313=ORIENTED_EDGE('',*,*,#4931,.T.);
#6314=ORIENTED_EDGE('',*,*,#4929,.T.);
#6315=ORIENTED_EDGE('',*,*,#4931,.F.);
#6316=ORIENTED_EDGE('',*,*,#4932,.F.);
#6317=ORIENTED_EDGE('',*,*,#4933,.T.);
#6318=ORIENTED_EDGE('',*,*,#4934,.T.);
#6319=ORIENTED_EDGE('',*,*,#4933,.F.);
#6320=ORIENTED_EDGE('',*,*,#4932,.T.);
#6321=ORIENTED_EDGE('',*,*,#4930,.T.);
#6322=ORIENTED_EDGE('',*,*,#4925,.T.);
#6323=ORIENTED_EDGE('',*,*,#4922,.T.);
#6324=ORIENTED_EDGE('',*,*,#4919,.T.);
#6325=ORIENTED_EDGE('',*,*,#4916,.T.);
#6326=ORIENTED_EDGE('',*,*,#4934,.F.);
#6327=ORIENTED_EDGE('',*,*,#4926,.T.);
#6328=ORIENTED_EDGE('',*,*,#4923,.T.);
#6329=ORIENTED_EDGE('',*,*,#4920,.T.);
#6330=ORIENTED_EDGE('',*,*,#4917,.T.);
#6331=ORIENTED_EDGE('',*,*,#4914,.T.);
#7608=CYLINDRICAL_SURFACE('',#9068,0.225);
#7609=CYLINDRICAL_SURFACE('',#9071,0.225);
#7610=CYLINDRICAL_SURFACE('',#9074,0.225);
#7611=CYLINDRICAL_SURFACE('',#9077,0.225);
#7612=CYLINDRICAL_SURFACE('',#9080,1.59);
#7613=CYLINDRICAL_SURFACE('',#9085,1.2);
#7614=CYLINDRICAL_SURFACE('',#9087,2.4);
#7855=ADVANCED_FACE('',(#1363),#7608,.F.);
#7856=ADVANCED_FACE('',(#1364),#7609,.F.);
#7857=ADVANCED_FACE('',(#1365),#7610,.F.);
#7858=ADVANCED_FACE('',(#1366),#7611,.F.);
#7859=ADVANCED_FACE('',(#1367),#7612,.T.);
#7860=ADVANCED_FACE('',(#1368,#848),#1029,.F.);
#7861=ADVANCED_FACE('',(#1369),#7613,.F.);
#7862=ADVANCED_FACE('',(#1370),#7614,.T.);
#7863=ADVANCED_FACE('',(#1371,#849,#850,#851,#852,#853),#1030,.T.);
#7864=ADVANCED_FACE('',(#1372,#854,#855,#856,#857,#858),#1031,.F.);
#8178=CLOSED_SHELL('',(#7855,#7856,#7857,#7858,#7859,#7860,#7861,#7862,
#7863,#7864));
#9067=AXIS2_PLACEMENT_3D('',#13174,#10645,#10646);
#9068=AXIS2_PLACEMENT_3D('',#13175,#10647,#10648);
#9069=AXIS2_PLACEMENT_3D('',#13177,#10649,#10650);
#9070=AXIS2_PLACEMENT_3D('',#13180,#10652,#10653);
#9071=AXIS2_PLACEMENT_3D('',#13181,#10654,#10655);
#9072=AXIS2_PLACEMENT_3D('',#13183,#10656,#10657);
#9073=AXIS2_PLACEMENT_3D('',#13186,#10659,#10660);
#9074=AXIS2_PLACEMENT_3D('',#13187,#10661,#10662);
#9075=AXIS2_PLACEMENT_3D('',#13189,#10663,#10664);
#9076=AXIS2_PLACEMENT_3D('',#13192,#10666,#10667);
#9077=AXIS2_PLACEMENT_3D('',#13193,#10668,#10669);
#9078=AXIS2_PLACEMENT_3D('',#13195,#10670,#10671);
#9079=AXIS2_PLACEMENT_3D('',#13198,#10673,#10674);
#9080=AXIS2_PLACEMENT_3D('',#13199,#10675,#10676);
#9081=AXIS2_PLACEMENT_3D('',#13201,#10677,#10678);
#9082=AXIS2_PLACEMENT_3D('',#13204,#10680,#10681);
#9083=AXIS2_PLACEMENT_3D('',#13205,#10682,#10683);
#9084=AXIS2_PLACEMENT_3D('',#13207,#10684,#10685);
#9085=AXIS2_PLACEMENT_3D('',#13208,#10686,#10687);
#9086=AXIS2_PLACEMENT_3D('',#13210,#10688,#10689);
#9087=AXIS2_PLACEMENT_3D('',#13212,#10691,#10692);
#9088=AXIS2_PLACEMENT_3D('',#13214,#10693,#10694);
#9089=AXIS2_PLACEMENT_3D('',#13217,#10696,#10697);
#9090=AXIS2_PLACEMENT_3D('',#13218,#10698,#10699);
#9091=AXIS2_PLACEMENT_3D('',#13219,#10700,#10701);
#10645=DIRECTION('axis',(0.,0.,1.));
#10646=DIRECTION('refdir',(1.,0.,0.));
#10647=DIRECTION('center_axis',(1.,0.,0.));
#10648=DIRECTION('ref_axis',(0.,0.,-1.));
#10649=DIRECTION('center_axis',(1.,0.,0.));
#10650=DIRECTION('ref_axis',(0.,0.,-1.));
#10651=DIRECTION('',(1.,0.,0.));
#10652=DIRECTION('center_axis',(-1.,0.,0.));
#10653=DIRECTION('ref_axis',(0.,0.,-1.));
#10654=DIRECTION('center_axis',(1.,0.,0.));
#10655=DIRECTION('ref_axis',(0.,0.,-1.));
#10656=DIRECTION('center_axis',(1.,0.,0.));
#10657=DIRECTION('ref_axis',(0.,0.,-1.));
#10658=DIRECTION('',(1.,0.,0.));
#10659=DIRECTION('center_axis',(-1.,0.,0.));
#10660=DIRECTION('ref_axis',(0.,0.,-1.));
#10661=DIRECTION('center_axis',(1.,0.,0.));
#10662=DIRECTION('ref_axis',(0.,0.,-1.));
#10663=DIRECTION('center_axis',(1.,0.,0.));
#10664=DIRECTION('ref_axis',(0.,0.,-1.));
#10665=DIRECTION('',(1.,0.,0.));
#10666=DIRECTION('center_axis',(-1.,0.,0.));
#10667=DIRECTION('ref_axis',(0.,0.,-1.));
#10668=DIRECTION('center_axis',(1.,0.,0.));
#10669=DIRECTION('ref_axis',(0.,0.,-1.));
#10670=DIRECTION('center_axis',(1.,0.,0.));
#10671=DIRECTION('ref_axis',(0.,0.,-1.));
#10672=DIRECTION('',(1.,0.,0.));
#10673=DIRECTION('center_axis',(-1.,0.,0.));
#10674=DIRECTION('ref_axis',(0.,0.,-1.));
#10675=DIRECTION('center_axis',(1.,0.,0.));
#10676=DIRECTION('ref_axis',(0.,0.,-1.));
#10677=DIRECTION('center_axis',(1.,0.,0.));
#10678=DIRECTION('ref_axis',(0.,0.,-1.));
#10679=DIRECTION('',(-1.,0.,0.));
#10680=DIRECTION('center_axis',(1.,0.,0.));
#10681=DIRECTION('ref_axis',(0.,0.,-1.));
#10682=DIRECTION('center_axis',(1.,0.,0.));
#10683=DIRECTION('ref_axis',(0.,0.,-1.));
#10684=DIRECTION('center_axis',(-1.,0.,0.));
#10685=DIRECTION('ref_axis',(0.,0.,-1.));
#10686=DIRECTION('center_axis',(1.,0.,0.));
#10687=DIRECTION('ref_axis',(0.,0.,-1.));
#10688=DIRECTION('center_axis',(-1.,0.,0.));
#10689=DIRECTION('ref_axis',(0.,0.,-1.));
#10690=DIRECTION('',(-1.,0.,0.));
#10691=DIRECTION('center_axis',(1.,0.,0.));
#10692=DIRECTION('ref_axis',(0.,0.,-1.));
#10693=DIRECTION('center_axis',(1.,0.,0.));
#10694=DIRECTION('ref_axis',(0.,0.,-1.));
#10695=DIRECTION('',(-1.,0.,0.));
#10696=DIRECTION('center_axis',(1.,0.,0.));
#10697=DIRECTION('ref_axis',(0.,0.,-1.));
#10698=DIRECTION('center_axis',(1.,0.,0.));
#10699=DIRECTION('ref_axis',(0.,0.,-1.));
#10700=DIRECTION('center_axis',(1.,0.,0.));
#10701=DIRECTION('ref_axis',(0.,0.,-1.));
#13174=CARTESIAN_POINT('',(0.,0.,0.));
#13175=CARTESIAN_POINT('Origin',(0.4,1.51507575950825,5.51507575950825));
#13176=CARTESIAN_POINT('',(0.5,1.51507575950825,5.74007575950825));
#13177=CARTESIAN_POINT('Origin',(0.5,1.51507575950825,5.51507575950825));
#13178=CARTESIAN_POINT('',(0.7,1.51507575950825,5.74007575950825));
#13179=CARTESIAN_POINT('',(0.4,1.51507575950825,5.74007575950825));
#13180=CARTESIAN_POINT('Origin',(0.7,1.51507575950825,5.51507575950825));
#13181=CARTESIAN_POINT('Origin',(0.4,1.51507575950825,8.48492424049175));
#13182=CARTESIAN_POINT('',(0.5,1.51507575950825,8.70992424049175));
#13183=CARTESIAN_POINT('Origin',(0.5,1.51507575950825,8.48492424049175));
#13184=CARTESIAN_POINT('',(0.7,1.51507575950825,8.70992424049175));
#13185=CARTESIAN_POINT('',(0.4,1.51507575950825,8.70992424049175));
#13186=CARTESIAN_POINT('Origin',(0.7,1.51507575950825,8.48492424049175));
#13187=CARTESIAN_POINT('Origin',(0.4,4.48492424049175,8.48492424049175));
#13188=CARTESIAN_POINT('',(0.5,4.48492424049175,8.70992424049175));
#13189=CARTESIAN_POINT('Origin',(0.5,4.48492424049175,8.48492424049175));
#13190=CARTESIAN_POINT('',(0.7,4.48492424049175,8.70992424049175));
#13191=CARTESIAN_POINT('',(0.4,4.48492424049175,8.70992424049175));
#13192=CARTESIAN_POINT('Origin',(0.7,4.48492424049175,8.48492424049175));
#13193=CARTESIAN_POINT('Origin',(0.4,4.48492424049175,5.51507575950825));
#13194=CARTESIAN_POINT('',(0.5,4.48492424049175,5.74007575950825));
#13195=CARTESIAN_POINT('Origin',(0.5,4.48492424049175,5.51507575950825));
#13196=CARTESIAN_POINT('',(0.7,4.48492424049175,5.74007575950825));
#13197=CARTESIAN_POINT('',(0.4,4.48492424049175,5.74007575950825));
#13198=CARTESIAN_POINT('Origin',(0.7,4.48492424049175,5.51507575950825));
#13199=CARTESIAN_POINT('Origin',(0.2,3.,7.));
#13200=CARTESIAN_POINT('',(0.5,3.,8.59));
#13201=CARTESIAN_POINT('Origin',(0.5,3.,7.));
#13202=CARTESIAN_POINT('',(0.2,3.,8.59));
#13203=CARTESIAN_POINT('',(0.2,3.,8.59));
#13204=CARTESIAN_POINT('Origin',(0.2,3.,7.));
#13205=CARTESIAN_POINT('Origin',(0.2,3.,7.));
#13206=CARTESIAN_POINT('',(0.2,3.,8.2));
#13207=CARTESIAN_POINT('Origin',(0.2,3.,7.));
#13208=CARTESIAN_POINT('Origin',(0.5,3.,7.));
#13209=CARTESIAN_POINT('',(0.7,3.,8.2));
#13210=CARTESIAN_POINT('Origin',(0.7,3.,7.));
#13211=CARTESIAN_POINT('',(0.5,3.,8.2));
#13212=CARTESIAN_POINT('Origin',(0.5,3.,7.));
#13213=CARTESIAN_POINT('',(0.7,3.,9.4));
#13214=CARTESIAN_POINT('Origin',(0.7,3.,7.));
#13215=CARTESIAN_POINT('',(0.5,3.,9.4));
#13216=CARTESIAN_POINT('',(0.5,3.,9.4));
#13217=CARTESIAN_POINT('Origin',(0.5,3.,7.));
#13218=CARTESIAN_POINT('Origin',(0.7,3.,7.));
#13219=CARTESIAN_POINT('Origin',(0.5,3.,7.));
#16955=UNCERTAINTY_MEASURE_WITH_UNIT(LENGTH_MEASURE(0.001),#17047,
'DISTANCE_ACCURACY_VALUE',
'Maximum model space distance between geometric entities at asserted c
onnectivities');
#16993=UNCERTAINTY_MEASURE_WITH_UNIT(LENGTH_MEASURE(0.001),#17047,
'DISTANCE_ACCURACY_VALUE',
'Maximum model space distance between geometric entities at asserted c
onnectivities');
#17008=(
GEOMETRIC_REPRESENTATION_CONTEXT(3)
GLOBAL_UNCERTAINTY_ASSIGNED_CONTEXT((#16955))
GLOBAL_UNIT_ASSIGNED_CONTEXT((#17047,#17049,#17050))
REPRESENTATION_CONTEXT('','3D')
);
#17046=(
GEOMETRIC_REPRESENTATION_CONTEXT(3)
GLOBAL_UNCERTAINTY_ASSIGNED_CONTEXT((#16993))
GLOBAL_UNIT_ASSIGNED_CONTEXT((#17047,#17049,#17050))
REPRESENTATION_CONTEXT('','3D')
);
#17047=(
LENGTH_UNIT()
NAMED_UNIT(*)
SI_UNIT(.CENTI.,.METRE.)
);
#17049=(
NAMED_UNIT(*)
PLANE_ANGLE_UNIT()
SI_UNIT($,.RADIAN.)
);
#17050=(
NAMED_UNIT(*)
SI_UNIT($,.STERADIAN.)
SOLID_ANGLE_UNIT()
);
#17065=SHAPE_DEFINITION_REPRESENTATION(#17117,#17272);
#17117=PRODUCT_DEFINITION_SHAPE('',$,#17325);
#17272=SHAPE_REPRESENTATION('',(#9067),#17008);
#17310=PRODUCT_DEFINITION_CONTEXT('part definition',#17468,'design');
#17325=PRODUCT_DEFINITION('Bearing cap (5)','Bearing cap (5)',#17377,#17310);
#17377=PRODUCT_DEFINITION_FORMATION('',$,#17484);
#17468=APPLICATION_CONTEXT(
'Core Data for Automotive Mechanical Design Process');
#17469=PRODUCT_CONTEXT('part definition',#17468,'mechanical');
#17484=PRODUCT('Bearing cap (5)','Bearing cap (5)','Bearing cap (5)',(#17469));
#17585=COLOUR_RGB('Grey',0.48,0.52,0.57);
#17586=FILL_AREA_STYLE_COLOUR('',#17585);
#17587=FILL_AREA_STYLE('',(#17586));
#17588=SURFACE_STYLE_FILL_AREA(#17587);
#17589=SURFACE_SIDE_STYLE('',(#17588));
#17590=SURFACE_STYLE_USAGE(.BOTH.,#17589);
#17591=PRESENTATION_STYLE_ASSIGNMENT((#17590));
ENDSEC;
END-ISO-10303-21;
